ISO-10303-21;
HEADER;
FILE_DESCRIPTION (('STEP AP214'),
    '1' );
FILE_NAME ('LEAD SCREW.step',
    '2026-10-09T16:01:55',
    ( '' ),
    ( '' ),
    'SwSTEP 2.0',
    'SolidWorks 2024',
    '' );
FILE_SCHEMA (( 'AUTOMOTIVE_DESIGN' ));
ENDSEC;

DATA;
#314=ORIENTED_EDGE ( 'NONE', *, *, #49490, .T. ) ;
#852=EDGE_CURVE ( 'NONE', #48338, #31486, #54371, .T. ) ;
#1211=CARTESIAN_POINT ( 'NONE',  ( 290.0000000000000000, 0.000000000000000000, 3.232999999999965901 ) ) ;
#1605=CARTESIAN_POINT ( 'NONE',  ( 289.2330000000000041, 4.898587196589412829E-16, -4.000000000000000000 ) ) ;
#1995=SHAPE_REPRESENTATION ( 'LEAD SCREW', ( #45918 ), #52770 ) ;
#2760=CARTESIAN_POINT ( 'NONE',  ( 289.2330000000000041, 4.898587196589412829E-16, 4.000000000000000000 ) ) ;
#3327=AXIS2_PLACEMENT_3D ( 'NONE', #14478, #24021, #51607 ) ;
#4122=ORIENTED_EDGE ( 'NONE', *, *, #9999, .F. ) ;
#4268=ORIENTED_EDGE ( 'NONE', *, *, #10077, .T. ) ;
#4643=CARTESIAN_POINT ( 'NONE',  ( 0.7669999999999959073, 0.000000000000000000, 0.000000000000000000 ) ) ;
#5069=( GEOMETRIC_REPRESENTATION_CONTEXT ( 3 ) GLOBAL_UNCERTAINTY_ASSIGNED_CONTEXT ( ( #30274 ) ) GLOBAL_UNIT_ASSIGNED_CONTEXT ( ( #5183, #54315, #21786 ) ) REPRESENTATION_CONTEXT ( 'NONE', 'WORKASPACE' ) );
#5183=( LENGTH_UNIT ( ) NAMED_UNIT ( * ) SI_UNIT ( .MILLI., .METRE. ) );
#5602=CONICAL_SURFACE ( 'NONE', #3327, 4.000000000000000000, 0.7853981633974730370 ) ;
#5621=AXIS2_PLACEMENT_3D ( 'NONE', #64277, #42348, #63928 ) ;
#5938=PLANE ( 'NONE',  #15057 ) ;
#6169=ORIENTED_EDGE ( 'NONE', *, *, #66081, .T. ) ;
#6239=AXIS2_PLACEMENT_3D ( 'NONE', #19966, #47544, #69110 ) ;
#6682=EDGE_LOOP ( 'NONE', ( #26285, #52428, #66221, #34161 ) ) ;
#8088=DIRECTION ( 'NONE',  ( 1.000000000000000000, -0.000000000000000000, -0.000000000000000000 ) ) ;
#8255=ORIENTED_EDGE ( 'NONE', *, *, #15129, .T. ) ;
#9523=ORIENTED_EDGE ( 'NONE', *, *, #42333, .T. ) ;
#9999=EDGE_CURVE ( 'NONE', #59753, #55220, #56492, .T. ) ;
#10077=EDGE_CURVE ( 'NONE', #55220, #48338, #37180, .T. ) ;
#10296=CARTESIAN_POINT ( 'NONE',  ( 0.000000000000000000, 3.959283101643393150E-16, 3.233000000000000096 ) ) ;
#10715=VECTOR ( 'NONE', #62451, 1000.000000000000000 ) ;
#10720=CONICAL_SURFACE ( 'NONE', #56985, 3.233000000000000096, 0.7853981633974362886 ) ;
#10974=ORIENTED_EDGE ( 'NONE', *, *, #42333, .F. ) ;
#11035=DIRECTION ( 'NONE',  ( 0.000000000000000000, 0.000000000000000000, -1.000000000000000000 ) ) ;
#11503=EDGE_CURVE ( 'NONE', #53184, #45669, #60258, .T. ) ;
#11744=LINE ( 'NONE', #37256, #50951 ) ;
#11865=LINE ( 'NONE', #1605, #19583 ) ;
#12405=EDGE_LOOP ( 'NONE', ( #19634, #58953, #314, #64627 ) ) ;
#13485=EDGE_LOOP ( 'NONE', ( #35075, #38129, #9523, #46703 ) ) ;
#13708=CLOSED_SHELL ( 'NONE', ( #39678, #17573, #61161, #40415, #52899, #67510, #53452, #43063 ) ) ;
#13882=DIRECTION ( 'NONE',  ( 0.000000000000000000, 0.000000000000000000, -1.000000000000000000 ) ) ;
#14478=CARTESIAN_POINT ( 'NONE',  ( 289.2330000000000041, 0.000000000000000000, 0.000000000000000000 ) ) ;
#14515=DIRECTION ( 'NONE',  ( 1.000000000000000000, 0.000000000000000000, 0.000000000000000000 ) ) ;
#14912=ADVANCED_BREP_SHAPE_REPRESENTATION ( '', ( #44296, #45918 ), #52770 ) ;
#15057=AXIS2_PLACEMENT_3D ( 'NONE', #16560, #26828, #42373 ) ;
#15129=EDGE_CURVE ( 'NONE', #31486, #48338, #38009, .T. ) ;
#15443=SURFACE_STYLE_USAGE ( .BOTH. , #37703 ) ;
#16085=ORIENTED_EDGE ( 'NONE', *, *, #31499, .T. ) ;
#16560=CARTESIAN_POINT ( 'NONE',  ( 290.0000000000000000, 3.233000000000000096, 0.000000000000000000 ) ) ;
#17573=ADVANCED_FACE ( 'NONE', ( #52871 ), #63106, .T. ) ;
#17699=AXIS2_PLACEMENT_3D ( 'NONE', #4643, #26207, #42467 ) ;
#17728=FACE_OUTER_BOUND ( 'NONE', #13485, .T. ) ;
#18092=LINE ( 'NONE', #23059, #29244 ) ;
#18127=CARTESIAN_POINT ( 'NONE',  ( 0.7669999999999959073, 0.000000000000000000, -3.999999999999977351 ) ) ;
#18706=DIRECTION ( 'NONE',  ( 0.000000000000000000, 0.000000000000000000, -1.000000000000000000 ) ) ;
#18776=CARTESIAN_POINT ( 'NONE',  ( 290.0000000000000000, 4.428935149116382035E-16, -3.232999999999965901 ) ) ;
#19039=SHAPE_DEFINITION_REPRESENTATION ( #29445, #1995 ) ;
#19072=FACE_OUTER_BOUND ( 'NONE', #20600, .T. ) ;
#19583=VECTOR ( 'NONE', #33098, 1000.000000000000000 ) ;
#19634=ORIENTED_EDGE ( 'NONE', *, *, #66081, .F. ) ;
#19966=CARTESIAN_POINT ( 'NONE',  ( 290.0000000000000000, 0.000000000000000000, 0.000000000000000000 ) ) ;
#20035=DIRECTION ( 'NONE',  ( 1.000000000000000000, -0.000000000000000000, -0.000000000000000000 ) ) ;
#20094=APPLICATION_CONTEXT ( 'automotive_design' ) ;
#20450=FACE_OUTER_BOUND ( 'NONE', #41281, .T. ) ;
#20600=EDGE_LOOP ( 'NONE', ( #54018, #6169, #37682, #31484 ) ) ;
#21637=DIRECTION ( 'NONE',  ( 0.000000000000000000, 0.000000000000000000, -1.000000000000000000 ) ) ;
#21786=( NAMED_UNIT ( * ) SI_UNIT ( $, .STERADIAN. ) SOLID_ANGLE_UNIT ( ) );
#21788=ORIENTED_EDGE ( 'NONE', *, *, #9999, .T. ) ;
#21941=CARTESIAN_POINT ( 'NONE',  ( 0.000000000000000000, 0.000000000000000000, 0.000000000000000000 ) ) ;
#22059=CARTESIAN_POINT ( 'NONE',  ( 0.7669999999999959073, 4.898587196589385219E-16, 3.999999999999977351 ) ) ;
#22775=CARTESIAN_POINT ( 'NONE',  ( 0.000000000000000000, 0.000000000000000000, 0.000000000000000000 ) ) ;
#23014=AXIS2_PLACEMENT_3D ( 'NONE', #65142, #69747, #11035 ) ;
#23059=CARTESIAN_POINT ( 'NONE',  ( 289.2330000000000041, 0.000000000000000000, 4.000000000000000000 ) ) ;
#23660=CARTESIAN_POINT ( 'NONE',  ( 289.2330000000000041, 0.000000000000000000, 0.000000000000000000 ) ) ;
#23754=AXIS2_PLACEMENT_3D ( 'NONE', #33436, #59264, #49689 ) ;
#24021=DIRECTION ( 'NONE',  ( -1.000000000000000000, 0.000000000000000000, 0.000000000000000000 ) ) ;
#24099=CARTESIAN_POINT ( 'NONE',  ( 289.2330000000000041, 0.000000000000000000, -4.000000000000000000 ) ) ;
#24155=FACE_OUTER_BOUND ( 'NONE', #6682, .T. ) ;
#25185=ORIENTED_EDGE ( 'NONE', *, *, #29624, .F. ) ;
#25560=DIRECTION ( 'NONE',  ( 1.000000000000000000, 0.000000000000000000, 0.000000000000000000 ) ) ;
#25713=FILL_AREA_STYLE ('',( #52578 ) ) ;
#26207=DIRECTION ( 'NONE',  ( 1.000000000000000000, 0.000000000000000000, 0.000000000000000000 ) ) ;
#26285=ORIENTED_EDGE ( 'NONE', *, *, #31499, .F. ) ;
#26568=CARTESIAN_POINT ( 'NONE',  ( 290.0000000000000000, 0.000000000000000000, 0.000000000000000000 ) ) ;
#26828=DIRECTION ( 'NONE',  ( -1.000000000000000000, 0.000000000000000000, 0.000000000000000000 ) ) ;
#27399=EDGE_LOOP ( 'NONE', ( #39024, #53183 ) ) ;
#27781=PLANE ( 'NONE',  #23754 ) ;
#29114=CARTESIAN_POINT ( 'NONE',  ( 290.0000000000000000, 0.000000000000000000, 0.000000000000000000 ) ) ;
#29244=VECTOR ( 'NONE', #64561, 1000.000000000000000 ) ;
#29277=( LENGTH_UNIT ( ) NAMED_UNIT ( * ) SI_UNIT ( .MILLI., .METRE. ) );
#29445=PRODUCT_DEFINITION_SHAPE ( 'NONE', 'NONE',  #38746 ) ;
#29624=EDGE_CURVE ( 'NONE', #45669, #53184, #39821, .T. ) ;
#30274=UNCERTAINTY_MEASURE_WITH_UNIT (LENGTH_MEASURE( 1.000000000000000082E-05 ), #5183, 'distance_accuracy_value', 'NONE');
#31484=ORIENTED_EDGE ( 'NONE', *, *, #49490, .F. ) ;
#31486=VERTEX_POINT ( 'NONE', #18127 ) ;
#31499=EDGE_CURVE ( 'NONE', #48338, #53184, #55619, .T. ) ;
#31727=EDGE_CURVE ( 'NONE', #55220, #59753, #52318, .T. ) ;
#32121=FACE_OUTER_BOUND ( 'NONE', #27399, .T. ) ;
#32355=DIRECTION ( 'NONE',  ( 1.000000000000000000, 0.000000000000000000, 0.000000000000000000 ) ) ;
#32404=PRESENTATION_STYLE_ASSIGNMENT (( #15443 ) ) ;
#33066=EDGE_CURVE ( 'NONE', #59339, #52255, #44446, .T. ) ;
#33098=DIRECTION ( 'NONE',  ( -0.7071067811865300312, 8.659560562355147330E-17, -0.7071067811865650032 ) ) ;
#33221=CARTESIAN_POINT ( 'NONE',  ( 0.000000000000000000, 0.000000000000000000, -3.233000000000000096 ) ) ;
#33436=CARTESIAN_POINT ( 'NONE',  ( 0.000000000000000000, 0.000000000000000000, 0.000000000000000000 ) ) ;
#34161=ORIENTED_EDGE ( 'NONE', *, *, #11503, .F. ) ;
#34232=( NAMED_UNIT ( * ) PLANE_ANGLE_UNIT ( ) SI_UNIT ( $, .RADIAN. ) );
#34539=CONICAL_SURFACE ( 'NONE', #67327, 3.233000000000000096, 0.7853981633974362886 ) ;
#35075=ORIENTED_EDGE ( 'NONE', *, *, #10077, .F. ) ;
#35628=CIRCLE ( 'NONE', #45781, 3.232999999999965901 ) ;
#35947=CARTESIAN_POINT ( 'NONE',  ( 289.2330000000000041, 0.000000000000000000, 0.000000000000000000 ) ) ;
#36431=DIRECTION ( 'NONE',  ( 0.000000000000000000, 0.000000000000000000, -1.000000000000000000 ) ) ;
#36830=DIRECTION ( 'NONE',  ( 0.000000000000000000, 0.000000000000000000, -1.000000000000000000 ) ) ;
#37180=LINE ( 'NONE', #10296, #62138 ) ;
#37256=CARTESIAN_POINT ( 'NONE',  ( 0.000000000000000000, 0.000000000000000000, -3.233000000000000096 ) ) ;
#37605=DIRECTION ( 'NONE',  ( 0.7071067811865560104, 0.000000000000000000, -0.7071067811865391350 ) ) ;
#37682=ORIENTED_EDGE ( 'NONE', *, *, #29624, .T. ) ;
#37703=SURFACE_SIDE_STYLE ('',( #42997 ) ) ;
#38009=CIRCLE ( 'NONE', #17699, 4.000000000000000000 ) ;
#38062=FACE_OUTER_BOUND ( 'NONE', #56686, .T. ) ;
#38129=ORIENTED_EDGE ( 'NONE', *, *, #31727, .T. ) ;
#38254=CARTESIAN_POINT ( 'NONE',  ( 0.000000000000000000, 0.000000000000000000, 0.000000000000000000 ) ) ;
#38746=PRODUCT_DEFINITION ( 'UNKNOWN', '', #41430, #62146 ) ;
#38970=STYLED_ITEM ( 'NONE', ( #32404 ), #44296 ) ;
#39024=ORIENTED_EDGE ( 'NONE', *, *, #43677, .T. ) ;
#39678=ADVANCED_FACE ( 'NONE', ( #19072 ), #5602, .T. ) ;
#39710=CYLINDRICAL_SURFACE ( 'NONE', #42398, 4.000000000000000000 ) ;
#39821=CIRCLE ( 'NONE', #40949, 4.000000000000000000 ) ;
#40168=PRODUCT ( 'LEAD SCREW', 'LEAD SCREW', '', ( #61830 ) ) ;
#40415=ADVANCED_FACE ( 'NONE', ( #38062 ), #27781, .F. ) ;
#40949=AXIS2_PLACEMENT_3D ( 'NONE', #35947, #20035, #57505 ) ;
#41281=EDGE_LOOP ( 'NONE', ( #21788, #4268, #50422, #10974 ) ) ;
#41430=PRODUCT_DEFINITION_FORMATION_WITH_SPECIFIED_SOURCE ( 'ANY', '', #40168, .NOT_KNOWN. ) ;
#41743=CONICAL_SURFACE ( 'NONE', #5621, 4.000000000000000000, 0.7853981633974730370 ) ;
#42333=EDGE_CURVE ( 'NONE', #59753, #31486, #11744, .T. ) ;
#42348=DIRECTION ( 'NONE',  ( -1.000000000000000000, 0.000000000000000000, 0.000000000000000000 ) ) ;
#42373=DIRECTION ( 'NONE',  ( 0.000000000000000000, 0.000000000000000000, 1.000000000000000000 ) ) ;
#42398=AXIS2_PLACEMENT_3D ( 'NONE', #29114, #67644, #57380 ) ;
#42467=DIRECTION ( 'NONE',  ( 0.000000000000000000, 0.000000000000000000, -1.000000000000000000 ) ) ;
#42697=FACE_OUTER_BOUND ( 'NONE', #12405, .T. ) ;
#42997=SURFACE_STYLE_FILL_AREA ( #25713 ) ;
#43063=ADVANCED_FACE ( 'NONE', ( #32121 ), #5938, .F. ) ;
#43224=( NAMED_UNIT ( * ) SI_UNIT ( $, .STERADIAN. ) SOLID_ANGLE_UNIT ( ) );
#43677=EDGE_CURVE ( 'NONE', #52255, #59339, #35628, .T. ) ;
#44184=EDGE_CURVE ( 'NONE', #31486, #45669, #63536, .T. ) ;
#44287=CARTESIAN_POINT ( 'NONE',  ( 0.000000000000000000, 4.428935149116389924E-16, 3.233000000000000096 ) ) ;
#44296=MANIFOLD_SOLID_BREP ( 'SAWC-0630-20060_welle', #13708 ) ;
#44446=CIRCLE ( 'NONE', #23014, 3.232999999999965901 ) ;
#45669=VERTEX_POINT ( 'NONE', #24099 ) ;
#45781=AXIS2_PLACEMENT_3D ( 'NONE', #26568, #48140, #54142 ) ;
#45918=AXIS2_PLACEMENT_3D ( 'NONE', #22775, #53934, #32355 ) ;
#46354=AXIS2_PLACEMENT_3D ( 'NONE', #21941, #58740, #36830 ) ;
#46610=CARTESIAN_POINT ( 'NONE',  ( 0.000000000000000000, 0.000000000000000000, 0.000000000000000000 ) ) ;
#46703=ORIENTED_EDGE ( 'NONE', *, *, #852, .F. ) ;
#47544=DIRECTION ( 'NONE',  ( 1.000000000000000000, 0.000000000000000000, 0.000000000000000000 ) ) ;
#47808=CARTESIAN_POINT ( 'NONE',  ( 0.7669999999999959073, 0.000000000000000000, 0.000000000000000000 ) ) ;
#48018=MECHANICAL_DESIGN_GEOMETRIC_PRESENTATION_REPRESENTATION('',(#38970),#5069);
#48140=DIRECTION ( 'NONE',  ( 1.000000000000000000, -0.000000000000000000, -0.000000000000000000 ) ) ;
#48338=VERTEX_POINT ( 'NONE', #22059 ) ;
#49490=EDGE_CURVE ( 'NONE', #52255, #53184, #18092, .T. ) ;
#49689=DIRECTION ( 'NONE',  ( 0.000000000000000000, 0.000000000000000000, -1.000000000000000000 ) ) ;
#50422=ORIENTED_EDGE ( 'NONE', *, *, #15129, .F. ) ;
#50951=VECTOR ( 'NONE', #37605, 999.9999999999998863 ) ;
#51607=DIRECTION ( 'NONE',  ( 0.000000000000000000, 0.000000000000000000, 1.000000000000000000 ) ) ;
#52255=VERTEX_POINT ( 'NONE', #1211 ) ;
#52318=CIRCLE ( 'NONE', #63633, 3.233000000000000096 ) ;
#52428=ORIENTED_EDGE ( 'NONE', *, *, #852, .T. ) ;
#52578=FILL_AREA_STYLE_COLOUR ( '', #69468 ) ;
#52770=( GEOMETRIC_REPRESENTATION_CONTEXT ( 3 ) GLOBAL_UNCERTAINTY_ASSIGNED_CONTEXT ( ( #64207 ) ) GLOBAL_UNIT_ASSIGNED_CONTEXT ( ( #29277, #34232, #43224 ) ) REPRESENTATION_CONTEXT ( 'NONE', 'WORKASPACE' ) );
#52871=FACE_OUTER_BOUND ( 'NONE', #66849, .T. ) ;
#52899=ADVANCED_FACE ( 'NONE', ( #17728 ), #10720, .T. ) ;
#53065=CARTESIAN_POINT ( 'NONE',  ( 0.000000000000000000, 0.000000000000000000, 0.000000000000000000 ) ) ;
#53183=ORIENTED_EDGE ( 'NONE', *, *, #33066, .T. ) ;
#53184=VERTEX_POINT ( 'NONE', #2760 ) ;
#53452=ADVANCED_FACE ( 'NONE', ( #42697 ), #41743, .T. ) ;
#53934=DIRECTION ( 'NONE',  ( 0.000000000000000000, 0.000000000000000000, 1.000000000000000000 ) ) ;
#54018=ORIENTED_EDGE ( 'NONE', *, *, #33066, .F. ) ;
#54142=DIRECTION ( 'NONE',  ( 0.000000000000000000, 0.000000000000000000, -1.000000000000000000 ) ) ;
#54315=( NAMED_UNIT ( * ) PLANE_ANGLE_UNIT ( ) SI_UNIT ( $, .RADIAN. ) );
#54371=CIRCLE ( 'NONE', #56622, 4.000000000000000000 ) ;
#55220=VERTEX_POINT ( 'NONE', #44287 ) ;
#55283=DIRECTION ( 'NONE',  ( 1.000000000000000000, 0.000000000000000000, 0.000000000000000000 ) ) ;
#55619=LINE ( 'NONE', #60913, #55638 ) ;
#55638=VECTOR ( 'NONE', #55283, 1000.000000000000000 ) ;
#56492=CIRCLE ( 'NONE', #46354, 3.233000000000000096 ) ;
#56622=AXIS2_PLACEMENT_3D ( 'NONE', #47808, #25560, #13882 ) ;
#56686=EDGE_LOOP ( 'NONE', ( #4122, #59297 ) ) ;
#56985=AXIS2_PLACEMENT_3D ( 'NONE', #53065, #14515, #36431 ) ;
#57380=DIRECTION ( 'NONE',  ( 0.000000000000000000, 0.000000000000000000, -1.000000000000000000 ) ) ;
#57505=DIRECTION ( 'NONE',  ( 0.000000000000000000, 0.000000000000000000, -1.000000000000000000 ) ) ;
#57579=DIRECTION ( 'NONE',  ( 0.000000000000000000, 0.000000000000000000, -1.000000000000000000 ) ) ;
#58740=DIRECTION ( 'NONE',  ( 1.000000000000000000, 0.000000000000000000, 0.000000000000000000 ) ) ;
#58953=ORIENTED_EDGE ( 'NONE', *, *, #43677, .F. ) ;
#59165=AXIS2_PLACEMENT_3D ( 'NONE', #23660, #8088, #18706 ) ;
#59264=DIRECTION ( 'NONE',  ( 1.000000000000000000, 0.000000000000000000, 0.000000000000000000 ) ) ;
#59297=ORIENTED_EDGE ( 'NONE', *, *, #31727, .F. ) ;
#59339=VERTEX_POINT ( 'NONE', #18776 ) ;
#59753=VERTEX_POINT ( 'NONE', #33221 ) ;
#59791=ORIENTED_EDGE ( 'NONE', *, *, #44184, .F. ) ;
#60258=CIRCLE ( 'NONE', #59165, 4.000000000000000000 ) ;
#60913=CARTESIAN_POINT ( 'NONE',  ( 290.0000000000000000, 4.898587196589412829E-16, 4.000000000000000000 ) ) ;
#61160=APPLICATION_CONTEXT ( 'automotive_design' ) ;
#61161=ADVANCED_FACE ( 'NONE', ( #20450 ), #34539, .T. ) ;
#61830=PRODUCT_CONTEXT ( 'NONE', #20094, 'mechanical' ) ;
#62138=VECTOR ( 'NONE', #63698, 999.9999999999998863 ) ;
#62146=PRODUCT_DEFINITION_CONTEXT ( 'detailed design', #61160, 'design' ) ;
#62451=DIRECTION ( 'NONE',  ( 1.000000000000000000, 0.000000000000000000, 0.000000000000000000 ) ) ;
#62517=DIRECTION ( 'NONE',  ( 1.000000000000000000, 0.000000000000000000, 0.000000000000000000 ) ) ;
#63106=CYLINDRICAL_SURFACE ( 'NONE', #6239, 4.000000000000000000 ) ;
#63172=CARTESIAN_POINT ( 'NONE',  ( 290.0000000000000000, 0.000000000000000000, -4.000000000000000000 ) ) ;
#63536=LINE ( 'NONE', #63172, #10715 ) ;
#63633=AXIS2_PLACEMENT_3D ( 'NONE', #38254, #64094, #21637 ) ;
#63698=DIRECTION ( 'NONE',  ( 0.7071067811865560104, 8.659560562354830553E-17, 0.7071067811865391350 ) ) ;
#63928=DIRECTION ( 'NONE',  ( 0.000000000000000000, 0.000000000000000000, 1.000000000000000000 ) ) ;
#64094=DIRECTION ( 'NONE',  ( 1.000000000000000000, 0.000000000000000000, 0.000000000000000000 ) ) ;
#64207=UNCERTAINTY_MEASURE_WITH_UNIT (LENGTH_MEASURE( 1.000000000000000082E-05 ), #29277, 'distance_accuracy_value', 'NONE');
#64277=CARTESIAN_POINT ( 'NONE',  ( 289.2330000000000041, 0.000000000000000000, 0.000000000000000000 ) ) ;
#64456=SHAPE_REPRESENTATION_RELATIONSHIP ( 'NONE' , 'NONE' ,  #1995, #14912 ) ;
#64561=DIRECTION ( 'NONE',  ( -0.7071067811865300312, 0.000000000000000000, 0.7071067811865650032 ) ) ;
#64627=ORIENTED_EDGE ( 'NONE', *, *, #11503, .T. ) ;
#65142=CARTESIAN_POINT ( 'NONE',  ( 290.0000000000000000, 0.000000000000000000, 0.000000000000000000 ) ) ;
#66081=EDGE_CURVE ( 'NONE', #59339, #45669, #11865, .T. ) ;
#66221=ORIENTED_EDGE ( 'NONE', *, *, #44184, .T. ) ;
#66849=EDGE_LOOP ( 'NONE', ( #8255, #16085, #25185, #59791 ) ) ;
#67327=AXIS2_PLACEMENT_3D ( 'NONE', #46610, #62517, #57579 ) ;
#67510=ADVANCED_FACE ( 'NONE', ( #24155 ), #39710, .T. ) ;
#67644=DIRECTION ( 'NONE',  ( 1.000000000000000000, 0.000000000000000000, 0.000000000000000000 ) ) ;
#69110=DIRECTION ( 'NONE',  ( 0.000000000000000000, 0.000000000000000000, -1.000000000000000000 ) ) ;
#69468=COLOUR_RGB ( '', 0.09019608, 0.27058824, 0.51372549) ;
#69747=DIRECTION ( 'NONE',  ( 1.000000000000000000, -0.000000000000000000, -0.000000000000000000 ) ) ;
ENDSEC;
END-ISO-10303-21;
